ISO-10303-21;
HEADER;
/* Generated by software containing ST-Developer
 * from STEP Tools, Inc. (www.steptools.com) 
 */

FILE_DESCRIPTION(
/* description */ ('PAT-091'),
/* implementation_level */ '2;1');

FILE_NAME(
/* name */ 'Axle distance sleeve 5 mm (1).step',
/* time_stamp */ '2026-10-27T15:34:44-07:00',
/* author */ (''),
/* organization */ (''),
/* preprocessor_version */ 'ST-DEVELOPER v20.2',
/* originating_system */ 'Autodesk Translation Framework v15.17.0.0',
/* authorisation */ '');

FILE_SCHEMA (('AUTOMOTIVE_DESIGN { 1 0 10303 214 3 1 1 }'));
ENDSEC;

DATA;
#10=MECHANICAL_DESIGN_GEOMETRIC_PRESENTATION_REPRESENTATION('',(#987),#25100);
#767=SHAPE_REPRESENTATION_RELATIONSHIP('SRR','None',#25528,#877);
#877=ADVANCED_BREP_SHAPE_REPRESENTATION('',(#1111),#24998);
#987=STYLED_ITEM('',(#26191),#1111);
#1111=MANIFOLD_SOLID_BREP('Body1',#13264);
#1331=FACE_BOUND('',#3138,.T.);
#1332=FACE_BOUND('',#3140,.T.);
#1706=PLANE('',#14892);
#1707=PLANE('',#14893);
#2201=FACE_OUTER_BOUND('',#3135,.T.);
#2202=FACE_OUTER_BOUND('',#3136,.T.);
#2203=FACE_OUTER_BOUND('',#3137,.T.);
#2204=FACE_OUTER_BOUND('',#3139,.T.);
#3135=EDGE_LOOP('',(#9572,#9573,#9574,#9575));
#3136=EDGE_LOOP('',(#9576,#9577,#9578,#9579));
#3137=EDGE_LOOP('',(#9580));
#3138=EDGE_LOOP('',(#9581));
#3139=EDGE_LOOP('',(#9582));
#3140=EDGE_LOOP('',(#9583));
#4280=LINE('',#21635,#5020);
#4281=LINE('',#21641,#5021);
#5020=VECTOR('',#17230,0.605);
#5021=VECTOR('',#17237,0.8);
#5748=CIRCLE('',#14887,0.605);
#5749=CIRCLE('',#14888,0.605);
#5750=CIRCLE('',#14890,0.8);
#5751=CIRCLE('',#14891,0.8);
#6583=VERTEX_POINT('',#21632);
#6584=VERTEX_POINT('',#21634);
#6585=VERTEX_POINT('',#21638);
#6586=VERTEX_POINT('',#21640);
#7721=EDGE_CURVE('',#6583,#6583,#5748,.T.);
#7722=EDGE_CURVE('',#6583,#6584,#4280,.T.);
#7723=EDGE_CURVE('',#6584,#6584,#5749,.T.);
#7724=EDGE_CURVE('',#6585,#6585,#5750,.T.);
#7725=EDGE_CURVE('',#6585,#6586,#4281,.T.);
#7726=EDGE_CURVE('',#6586,#6586,#5751,.T.);
#9572=ORIENTED_EDGE('',*,*,#7721,.F.);
#9573=ORIENTED_EDGE('',*,*,#7722,.T.);
#9574=ORIENTED_EDGE('',*,*,#7723,.T.);
#9575=ORIENTED_EDGE('',*,*,#7722,.F.);
#9576=ORIENTED_EDGE('',*,*,#7724,.F.);
#9577=ORIENTED_EDGE('',*,*,#7725,.T.);
#9578=ORIENTED_EDGE('',*,*,#7726,.T.);
#9579=ORIENTED_EDGE('',*,*,#7725,.F.);
#9580=ORIENTED_EDGE('',*,*,#7724,.T.);
#9581=ORIENTED_EDGE('',*,*,#7721,.T.);
#9582=ORIENTED_EDGE('',*,*,#7726,.F.);
#9583=ORIENTED_EDGE('',*,*,#7723,.F.);
#12146=CYLINDRICAL_SURFACE('',#14886,0.605);
#12147=CYLINDRICAL_SURFACE('',#14889,0.8);
#12568=ADVANCED_FACE('',(#2201),#12146,.F.);
#12569=ADVANCED_FACE('',(#2202),#12147,.T.);
#12570=ADVANCED_FACE('',(#2203,#1331),#1706,.T.);
#12571=ADVANCED_FACE('',(#2204,#1332),#1707,.F.);
#13264=CLOSED_SHELL('',(#12568,#12569,#12570,#12571));
#14885=AXIS2_PLACEMENT_3D('',#21630,#17224,#17225);
#14886=AXIS2_PLACEMENT_3D('',#21631,#17226,#17227);
#14887=AXIS2_PLACEMENT_3D('',#21633,#17228,#17229);
#14888=AXIS2_PLACEMENT_3D('',#21636,#17231,#17232);
#14889=AXIS2_PLACEMENT_3D('',#21637,#17233,#17234);
#14890=AXIS2_PLACEMENT_3D('',#21639,#17235,#17236);
#14891=AXIS2_PLACEMENT_3D('',#21642,#17238,#17239);
#14892=AXIS2_PLACEMENT_3D('',#21643,#17240,#17241);
#14893=AXIS2_PLACEMENT_3D('',#21644,#17242,#17243);
#17224=DIRECTION('axis',(0.,0.,1.));
#17225=DIRECTION('refdir',(1.,0.,0.));
#17226=DIRECTION('center_axis',(0.,1.,0.));
#17227=DIRECTION('ref_axis',(1.,0.,0.));
#17228=DIRECTION('center_axis',(0.,-1.,0.));
#17229=DIRECTION('ref_axis',(1.,0.,0.));
#17230=DIRECTION('',(0.,-1.,0.));
#17231=DIRECTION('center_axis',(0.,-1.,0.));
#17232=DIRECTION('ref_axis',(1.,0.,0.));
#17233=DIRECTION('center_axis',(0.,1.,0.));
#17234=DIRECTION('ref_axis',(1.,0.,0.));
#17235=DIRECTION('center_axis',(0.,1.,0.));
#17236=DIRECTION('ref_axis',(1.,0.,0.));
#17237=DIRECTION('',(0.,-1.,0.));
#17238=DIRECTION('center_axis',(0.,1.,0.));
#17239=DIRECTION('ref_axis',(1.,0.,0.));
#17240=DIRECTION('center_axis',(0.,1.,0.));
#17241=DIRECTION('ref_axis',(1.,0.,0.));
#17242=DIRECTION('center_axis',(0.,1.,0.));
#17243=DIRECTION('ref_axis',(1.,0.,0.));
#21630=CARTESIAN_POINT('',(0.,0.,0.));
#21631=CARTESIAN_POINT('Origin',(0.,6.,3.));
#21632=CARTESIAN_POINT('',(-0.605,6.5,3.));
#21633=CARTESIAN_POINT('Origin',(0.,6.5,3.));
#21634=CARTESIAN_POINT('',(-0.605,6.,3.));
#21635=CARTESIAN_POINT('',(-0.605,6.,3.));
#21636=CARTESIAN_POINT('Origin',(0.,6.,3.));
#21637=CARTESIAN_POINT('Origin',(0.,6.,3.));
#21638=CARTESIAN_POINT('',(-0.8,6.5,3.));
#21639=CARTESIAN_POINT('Origin',(0.,6.5,3.));
#21640=CARTESIAN_POINT('',(-0.8,6.,3.));
#21641=CARTESIAN_POINT('',(-0.8,6.,3.));
#21642=CARTESIAN_POINT('Origin',(0.,6.,3.));
#21643=CARTESIAN_POINT('Origin',(0.,6.5,3.));
#21644=CARTESIAN_POINT('Origin',(0.,6.,3.));
#24877=UNCERTAINTY_MEASURE_WITH_UNIT(LENGTH_MEASURE(0.001),#25101,
'DISTANCE_ACCURACY_VALUE',
'Maximum model space distance between geometric entities at asserted c
onnectivities');
#24979=UNCERTAINTY_MEASURE_WITH_UNIT(LENGTH_MEASURE(0.001),#25101,
'DISTANCE_ACCURACY_VALUE',
'Maximum model space distance between geometric entities at asserted c
onnectivities');
#24998=(
GEOMETRIC_REPRESENTATION_CONTEXT(3)
GLOBAL_UNCERTAINTY_ASSIGNED_CONTEXT((#24877))
GLOBAL_UNIT_ASSIGNED_CONTEXT((#25101,#25103,#25104))
REPRESENTATION_CONTEXT('','3D')
);
#25100=(
GEOMETRIC_REPRESENTATION_CONTEXT(3)
GLOBAL_UNCERTAINTY_ASSIGNED_CONTEXT((#24979))
GLOBAL_UNIT_ASSIGNED_CONTEXT((#25101,#25103,#25104))
REPRESENTATION_CONTEXT('','3D')
);
#25101=(
LENGTH_UNIT()
NAMED_UNIT(*)
SI_UNIT(.CENTI.,.METRE.)
);
#25103=(
NAMED_UNIT(*)
PLANE_ANGLE_UNIT()
SI_UNIT($,.RADIAN.)
);
#25104=(
NAMED_UNIT(*)
SI_UNIT($,.STERADIAN.)
SOLID_ANGLE_UNIT()
);
#25123=SHAPE_DEFINITION_REPRESENTATION(#25243,#25528);
#25243=PRODUCT_DEFINITION_SHAPE('',$,#25649);
#25528=SHAPE_REPRESENTATION('',(#14885),#24998);
#25630=PRODUCT_DEFINITION_CONTEXT('part definition',#25992,'design');
#25649=PRODUCT_DEFINITION('Axle distance sleeve 5 mm (1)',
'Axle distance sleeve 5 mm (1)',#25769,#25630);
#25769=PRODUCT_DEFINITION_FORMATION('',$,#26012);
#25992=APPLICATION_CONTEXT(
'Core Data for Automotive Mechanical Design Process');
#25993=PRODUCT_CONTEXT('part definition',#25992,'mechanical');
#26012=PRODUCT('Axle distance sleeve 5 mm (1)',
'Axle distance sleeve 5 mm (1)','Axle distance sleeve 5 mm (1)',(#25993));
#26185=COLOUR_RGB('Grey',0.48,0.52,0.57);
#26186=FILL_AREA_STYLE_COLOUR('',#26185);
#26187=FILL_AREA_STYLE('',(#26186));
#26188=SURFACE_STYLE_FILL_AREA(#26187);
#26189=SURFACE_SIDE_STYLE('',(#26188));
#26190=SURFACE_STYLE_USAGE(.BOTH.,#26189);
#26191=PRESENTATION_STYLE_ASSIGNMENT((#26190));
ENDSEC;
END-ISO-10303-21;
